ISO-10303-21;
HEADER;
/* Generated by software containing ST-Developer
 * from STEP Tools, Inc. (www.steptools.com) 
 */

FILE_DESCRIPTION(
/* description */ ('Rigid flange shaft coupling assembly'),
/* implementation_level */ '2;1');

FILE_NAME(
/* name */ 'Flat Washer - M8.step',
/* time_stamp */ '2026-10-27T10:47:16-07:00',
/* author */ (''),
/* organization */ (''),
/* preprocessor_version */ 'ST-DEVELOPER v20.2',
/* originating_system */ 'Autodesk Translation Framework v15.17.0.0',
/* authorisation */ '');

FILE_SCHEMA (('AUTOMOTIVE_DESIGN { 1 0 10303 214 3 1 1 }'));
ENDSEC;

DATA;
#10=MECHANICAL_DESIGN_GEOMETRIC_PRESENTATION_REPRESENTATION('',(#410),#9141);
#353=SHAPE_REPRESENTATION_RELATIONSHIP('SRR','None',#9288,#381);
#381=ADVANCED_BREP_SHAPE_REPRESENTATION('',(#439),#9123);
#410=STYLED_ITEM('',(#9507),#439);
#439=MANIFOLD_SOLID_BREP('Body1',#4764);
#514=FACE_BOUND('',#1179,.T.);
#515=FACE_BOUND('',#1181,.T.);
#632=PLANE('',#5281);
#633=PLANE('',#5282);
#843=FACE_OUTER_BOUND('',#1176,.T.);
#844=FACE_OUTER_BOUND('',#1177,.T.);
#845=FACE_OUTER_BOUND('',#1178,.T.);
#846=FACE_OUTER_BOUND('',#1180,.T.);
#1176=EDGE_LOOP('',(#3695,#3696,#3697,#3698));
#1177=EDGE_LOOP('',(#3699,#3700,#3701,#3702));
#1178=EDGE_LOOP('',(#3703));
#1179=EDGE_LOOP('',(#3704));
#1180=EDGE_LOOP('',(#3705));
#1181=EDGE_LOOP('',(#3706));
#1541=LINE('',#7997,#1886);
#1542=LINE('',#8003,#1887);
#1886=VECTOR('',#6146,0.42);
#1887=VECTOR('',#6153,0.8);
#2161=CIRCLE('',#5276,0.42);
#2162=CIRCLE('',#5277,0.42);
#2163=CIRCLE('',#5279,0.8);
#2164=CIRCLE('',#5280,0.8);
#2434=VERTEX_POINT('',#7994);
#2435=VERTEX_POINT('',#7996);
#2436=VERTEX_POINT('',#8000);
#2437=VERTEX_POINT('',#8002);
#2891=EDGE_CURVE('',#2434,#2434,#2161,.T.);
#2892=EDGE_CURVE('',#2434,#2435,#1541,.T.);
#2893=EDGE_CURVE('',#2435,#2435,#2162,.T.);
#2894=EDGE_CURVE('',#2436,#2436,#2163,.T.);
#2895=EDGE_CURVE('',#2436,#2437,#1542,.T.);
#2896=EDGE_CURVE('',#2437,#2437,#2164,.T.);
#3695=ORIENTED_EDGE('',*,*,#2891,.F.);
#3696=ORIENTED_EDGE('',*,*,#2892,.T.);
#3697=ORIENTED_EDGE('',*,*,#2893,.T.);
#3698=ORIENTED_EDGE('',*,*,#2892,.F.);
#3699=ORIENTED_EDGE('',*,*,#2894,.F.);
#3700=ORIENTED_EDGE('',*,*,#2895,.T.);
#3701=ORIENTED_EDGE('',*,*,#2896,.T.);
#3702=ORIENTED_EDGE('',*,*,#2895,.F.);
#3703=ORIENTED_EDGE('',*,*,#2894,.T.);
#3704=ORIENTED_EDGE('',*,*,#2891,.T.);
#3705=ORIENTED_EDGE('',*,*,#2896,.F.);
#3706=ORIENTED_EDGE('',*,*,#2893,.F.);
#4434=CYLINDRICAL_SURFACE('',#5275,0.42);
#4435=CYLINDRICAL_SURFACE('',#5278,0.8);
#4579=ADVANCED_FACE('',(#843),#4434,.F.);
#4580=ADVANCED_FACE('',(#844),#4435,.T.);
#4581=ADVANCED_FACE('',(#845,#514),#632,.T.);
#4582=ADVANCED_FACE('',(#846,#515),#633,.F.);
#4764=CLOSED_SHELL('',(#4579,#4580,#4581,#4582));
#5274=AXIS2_PLACEMENT_3D('',#7992,#6140,#6141);
#5275=AXIS2_PLACEMENT_3D('',#7993,#6142,#6143);
#5276=AXIS2_PLACEMENT_3D('',#7995,#6144,#6145);
#5277=AXIS2_PLACEMENT_3D('',#7998,#6147,#6148);
#5278=AXIS2_PLACEMENT_3D('',#7999,#6149,#6150);
#5279=AXIS2_PLACEMENT_3D('',#8001,#6151,#6152);
#5280=AXIS2_PLACEMENT_3D('',#8004,#6154,#6155);
#5281=AXIS2_PLACEMENT_3D('',#8005,#6156,#6157);
#5282=AXIS2_PLACEMENT_3D('',#8006,#6158,#6159);
#6140=DIRECTION('axis',(0.,0.,1.));
#6141=DIRECTION('refdir',(1.,0.,0.));
#6142=DIRECTION('center_axis',(0.,1.,0.));
#6143=DIRECTION('ref_axis',(1.,0.,0.));
#6144=DIRECTION('center_axis',(0.,-1.,0.));
#6145=DIRECTION('ref_axis',(1.,0.,0.));
#6146=DIRECTION('',(0.,-1.,0.));
#6147=DIRECTION('center_axis',(0.,-1.,0.));
#6148=DIRECTION('ref_axis',(1.,0.,0.));
#6149=DIRECTION('center_axis',(0.,1.,0.));
#6150=DIRECTION('ref_axis',(1.,0.,0.));
#6151=DIRECTION('center_axis',(0.,1.,0.));
#6152=DIRECTION('ref_axis',(1.,0.,0.));
#6153=DIRECTION('',(0.,-1.,0.));
#6154=DIRECTION('center_axis',(0.,1.,0.));
#6155=DIRECTION('ref_axis',(1.,0.,0.));
#6156=DIRECTION('center_axis',(0.,1.,0.));
#6157=DIRECTION('ref_axis',(1.,0.,0.));
#6158=DIRECTION('center_axis',(0.,1.,0.));
#6159=DIRECTION('ref_axis',(1.,0.,0.));
#7992=CARTESIAN_POINT('',(0.,0.,0.));
#7993=CARTESIAN_POINT('Origin',(0.,0.,0.));
#7994=CARTESIAN_POINT('',(-0.42,0.16,5.14351655641888E-17));
#7995=CARTESIAN_POINT('Origin',(0.,0.16,0.));
#7996=CARTESIAN_POINT('',(-0.42,0.,5.14351655641888E-17));
#7997=CARTESIAN_POINT('',(-0.42,0.,5.14351655641888E-17));
#7998=CARTESIAN_POINT('Origin',(0.,0.,0.));
#7999=CARTESIAN_POINT('Origin',(0.,0.,0.));
#8000=CARTESIAN_POINT('',(-0.8,0.16,9.79717439317883E-17));
#8001=CARTESIAN_POINT('Origin',(0.,0.16,0.));
#8002=CARTESIAN_POINT('',(-0.8,0.,9.79717439317883E-17));
#8003=CARTESIAN_POINT('',(-0.8,0.,9.79717439317883E-17));
#8004=CARTESIAN_POINT('Origin',(0.,0.,0.));
#8005=CARTESIAN_POINT('Origin',(0.,0.16,0.));
#8006=CARTESIAN_POINT('Origin',(0.,0.,0.));
#9090=UNCERTAINTY_MEASURE_WITH_UNIT(LENGTH_MEASURE(0.001),#9142,
'DISTANCE_ACCURACY_VALUE',
'Maximum model space distance between geometric entities at asserted c
onnectivities');
#9108=UNCERTAINTY_MEASURE_WITH_UNIT(LENGTH_MEASURE(0.001),#9142,
'DISTANCE_ACCURACY_VALUE',
'Maximum model space distance between geometric entities at asserted c
onnectivities');
#9123=(
GEOMETRIC_REPRESENTATION_CONTEXT(3)
GLOBAL_UNCERTAINTY_ASSIGNED_CONTEXT((#9090))
GLOBAL_UNIT_ASSIGNED_CONTEXT((#9142,#9144,#9145))
REPRESENTATION_CONTEXT('','3D')
);
#9141=(
GEOMETRIC_REPRESENTATION_CONTEXT(3)
GLOBAL_UNCERTAINTY_ASSIGNED_CONTEXT((#9108))
GLOBAL_UNIT_ASSIGNED_CONTEXT((#9142,#9144,#9145))
REPRESENTATION_CONTEXT('','3D')
);
#9142=(
LENGTH_UNIT()
NAMED_UNIT(*)
SI_UNIT(.CENTI.,.METRE.)
);
#9144=(
NAMED_UNIT(*)
PLANE_ANGLE_UNIT()
SI_UNIT($,.RADIAN.)
);
#9145=(
NAMED_UNIT(*)
SI_UNIT($,.STERADIAN.)
SOLID_ANGLE_UNIT()
);
#9160=SHAPE_DEFINITION_REPRESENTATION(#9194,#9288);
#9194=PRODUCT_DEFINITION_SHAPE('',$,#9321);
#9288=SHAPE_REPRESENTATION('',(#5274),#9123);
#9306=PRODUCT_DEFINITION_CONTEXT('part definition',#9404,'design');
#9321=PRODUCT_DEFINITION('Flat Washer - M8','Flat Washer - M8',#9353,#9306);
#9353=PRODUCT_DEFINITION_FORMATION('',$,#9420);
#9404=APPLICATION_CONTEXT(
'Core Data for Automotive Mechanical Design Process');
#9405=PRODUCT_CONTEXT('part definition',#9404,'mechanical');
#9420=PRODUCT('Flat Washer - M8','Flat Washer - M8','Flat Washer - M8',
(#9405));
#9501=COLOUR_RGB('Black',0.12,0.14,0.17);
#9502=FILL_AREA_STYLE_COLOUR('',#9501);
#9503=FILL_AREA_STYLE('',(#9502));
#9504=SURFACE_STYLE_FILL_AREA(#9503);
#9505=SURFACE_SIDE_STYLE('',(#9504));
#9506=SURFACE_STYLE_USAGE(.BOTH.,#9505);
#9507=PRESENTATION_STYLE_ASSIGNMENT((#9506));
ENDSEC;
END-ISO-10303-21;
